ISO-10303-21;
HEADER;
/* Generated by software containing ST-Developer
 * from STEP Tools, Inc. (www.steptools.com) 
 */

FILE_DESCRIPTION(
/* description */ ('Flywheel Crank-Slider'),
/* implementation_level */ '2;1');

FILE_NAME(
/* name */ 'Foot strip (1).step',
/* time_stamp */ '2026-10-28T03:23:13-07:00',
/* author */ (''),
/* organization */ (''),
/* preprocessor_version */ 'ST-DEVELOPER v20.2',
/* originating_system */ 'Autodesk Translation Framework v15.17.0.0',
/* authorisation */ '');

FILE_SCHEMA (('AUTOMOTIVE_DESIGN { 1 0 10303 214 3 1 1 }'));
ENDSEC;

DATA;
#10=MECHANICAL_DESIGN_GEOMETRIC_PRESENTATION_REPRESENTATION('',(#678),#17322);
#574=SHAPE_REPRESENTATION_RELATIONSHIP('SRR','None',#17570,#626);
#626=ADVANCED_BREP_SHAPE_REPRESENTATION('',(#739),#17274);
#678=STYLED_ITEM('',(#17917),#739);
#739=MANIFOLD_SOLID_BREP('Body1',#9056);
#1079=PLANE('',#9940);
#1080=PLANE('',#9941);
#1081=PLANE('',#9942);
#1082=PLANE('',#9943);
#1083=PLANE('',#9944);
#1084=PLANE('',#9945);
#1446=FACE_OUTER_BOUND('',#2057,.T.);
#1447=FACE_OUTER_BOUND('',#2058,.T.);
#1448=FACE_OUTER_BOUND('',#2059,.T.);
#1449=FACE_OUTER_BOUND('',#2060,.T.);
#1450=FACE_OUTER_BOUND('',#2061,.T.);
#1451=FACE_OUTER_BOUND('',#2062,.T.);
#2057=EDGE_LOOP('',(#6630,#6631,#6632,#6633));
#2058=EDGE_LOOP('',(#6634,#6635,#6636,#6637));
#2059=EDGE_LOOP('',(#6638,#6639,#6640,#6641));
#2060=EDGE_LOOP('',(#6642,#6643,#6644,#6645));
#2061=EDGE_LOOP('',(#6646,#6647,#6648,#6649));
#2062=EDGE_LOOP('',(#6650,#6651,#6652,#6653));
#2754=LINE('',#14291,#3365);
#2755=LINE('',#14293,#3366);
#2756=LINE('',#14295,#3367);
#2757=LINE('',#14296,#3368);
#2758=LINE('',#14299,#3369);
#2759=LINE('',#14301,#3370);
#2760=LINE('',#14302,#3371);
#2761=LINE('',#14305,#3372);
#2762=LINE('',#14307,#3373);
#2763=LINE('',#14308,#3374);
#2764=LINE('',#14310,#3375);
#2765=LINE('',#14311,#3376);
#3365=VECTOR('',#11480,1.);
#3366=VECTOR('',#11481,1.);
#3367=VECTOR('',#11482,1.);
#3368=VECTOR('',#11483,1.);
#3369=VECTOR('',#11486,1.);
#3370=VECTOR('',#11487,1.);
#3371=VECTOR('',#11488,1.);
#3372=VECTOR('',#11491,1.);
#3373=VECTOR('',#11492,1.);
#3374=VECTOR('',#11493,1.);
#3375=VECTOR('',#11496,1.);
#3376=VECTOR('',#11497,1.);
#4441=VERTEX_POINT('',#14289);
#4442=VERTEX_POINT('',#14290);
#4443=VERTEX_POINT('',#14292);
#4444=VERTEX_POINT('',#14294);
#4445=VERTEX_POINT('',#14298);
#4446=VERTEX_POINT('',#14300);
#4447=VERTEX_POINT('',#14304);
#4448=VERTEX_POINT('',#14306);
#5272=EDGE_CURVE('',#4441,#4442,#2754,.T.);
#5273=EDGE_CURVE('',#4442,#4443,#2755,.T.);
#5274=EDGE_CURVE('',#4444,#4443,#2756,.T.);
#5275=EDGE_CURVE('',#4441,#4444,#2757,.T.);
#5276=EDGE_CURVE('',#4445,#4441,#2758,.T.);
#5277=EDGE_CURVE('',#4446,#4444,#2759,.T.);
#5278=EDGE_CURVE('',#4445,#4446,#2760,.T.);
#5279=EDGE_CURVE('',#4447,#4445,#2761,.T.);
#5280=EDGE_CURVE('',#4448,#4446,#2762,.T.);
#5281=EDGE_CURVE('',#4447,#4448,#2763,.T.);
#5282=EDGE_CURVE('',#4442,#4447,#2764,.T.);
#5283=EDGE_CURVE('',#4443,#4448,#2765,.T.);
#6630=ORIENTED_EDGE('',*,*,#5272,.T.);
#6631=ORIENTED_EDGE('',*,*,#5273,.T.);
#6632=ORIENTED_EDGE('',*,*,#5274,.F.);
#6633=ORIENTED_EDGE('',*,*,#5275,.F.);
#6634=ORIENTED_EDGE('',*,*,#5276,.T.);
#6635=ORIENTED_EDGE('',*,*,#5275,.T.);
#6636=ORIENTED_EDGE('',*,*,#5277,.F.);
#6637=ORIENTED_EDGE('',*,*,#5278,.F.);
#6638=ORIENTED_EDGE('',*,*,#5279,.T.);
#6639=ORIENTED_EDGE('',*,*,#5278,.T.);
#6640=ORIENTED_EDGE('',*,*,#5280,.F.);
#6641=ORIENTED_EDGE('',*,*,#5281,.F.);
#6642=ORIENTED_EDGE('',*,*,#5282,.T.);
#6643=ORIENTED_EDGE('',*,*,#5281,.T.);
#6644=ORIENTED_EDGE('',*,*,#5283,.F.);
#6645=ORIENTED_EDGE('',*,*,#5273,.F.);
#6646=ORIENTED_EDGE('',*,*,#5283,.T.);
#6647=ORIENTED_EDGE('',*,*,#5280,.T.);
#6648=ORIENTED_EDGE('',*,*,#5277,.T.);
#6649=ORIENTED_EDGE('',*,*,#5274,.T.);
#6650=ORIENTED_EDGE('',*,*,#5282,.F.);
#6651=ORIENTED_EDGE('',*,*,#5272,.F.);
#6652=ORIENTED_EDGE('',*,*,#5276,.F.);
#6653=ORIENTED_EDGE('',*,*,#5279,.F.);
#8637=ADVANCED_FACE('',(#1446),#1079,.T.);
#8638=ADVANCED_FACE('',(#1447),#1080,.T.);
#8639=ADVANCED_FACE('',(#1448),#1081,.T.);
#8640=ADVANCED_FACE('',(#1449),#1082,.T.);
#8641=ADVANCED_FACE('',(#1450),#1083,.T.);
#8642=ADVANCED_FACE('',(#1451),#1084,.F.);
#9056=CLOSED_SHELL('',(#8637,#8638,#8639,#8640,#8641,#8642));
#9939=AXIS2_PLACEMENT_3D('',#14287,#11476,#11477);
#9940=AXIS2_PLACEMENT_3D('',#14288,#11478,#11479);
#9941=AXIS2_PLACEMENT_3D('',#14297,#11484,#11485);
#9942=AXIS2_PLACEMENT_3D('',#14303,#11489,#11490);
#9943=AXIS2_PLACEMENT_3D('',#14309,#11494,#11495);
#9944=AXIS2_PLACEMENT_3D('',#14312,#11498,#11499);
#9945=AXIS2_PLACEMENT_3D('',#14313,#11500,#11501);
#11476=DIRECTION('axis',(0.,0.,1.));
#11477=DIRECTION('refdir',(1.,0.,0.));
#11478=DIRECTION('center_axis',(0.,1.,0.));
#11479=DIRECTION('ref_axis',(-1.,0.,0.));
#11480=DIRECTION('',(-1.,0.,0.));
#11481=DIRECTION('',(0.,0.,1.));
#11482=DIRECTION('',(-1.,0.,0.));
#11483=DIRECTION('',(0.,0.,1.));
#11484=DIRECTION('center_axis',(1.,0.,0.));
#11485=DIRECTION('ref_axis',(0.,1.,0.));
#11486=DIRECTION('',(0.,1.,0.));
#11487=DIRECTION('',(0.,1.,0.));
#11488=DIRECTION('',(0.,0.,1.));
#11489=DIRECTION('center_axis',(0.,-1.,0.));
#11490=DIRECTION('ref_axis',(1.,0.,0.));
#11491=DIRECTION('',(1.,0.,0.));
#11492=DIRECTION('',(1.,0.,0.));
#11493=DIRECTION('',(0.,0.,1.));
#11494=DIRECTION('center_axis',(-1.,0.,0.));
#11495=DIRECTION('ref_axis',(0.,-1.,0.));
#11496=DIRECTION('',(0.,-1.,0.));
#11497=DIRECTION('',(0.,-1.,0.));
#11498=DIRECTION('center_axis',(0.,0.,1.));
#11499=DIRECTION('ref_axis',(1.,0.,0.));
#11500=DIRECTION('center_axis',(0.,0.,1.));
#11501=DIRECTION('ref_axis',(1.,0.,0.));
#14287=CARTESIAN_POINT('',(0.,0.,0.));
#14288=CARTESIAN_POINT('Origin',(24.,9.,-0.5));
#14289=CARTESIAN_POINT('',(24.,9.,-0.5));
#14290=CARTESIAN_POINT('',(22.,9.,-0.5));
#14291=CARTESIAN_POINT('',(24.,9.,-0.5));
#14292=CARTESIAN_POINT('',(22.,9.,0.));
#14293=CARTESIAN_POINT('',(22.,9.,-0.5));
#14294=CARTESIAN_POINT('',(24.,9.,0.));
#14295=CARTESIAN_POINT('',(24.,9.,0.));
#14296=CARTESIAN_POINT('',(24.,9.,-0.5));
#14297=CARTESIAN_POINT('Origin',(24.,-18.,-0.5));
#14298=CARTESIAN_POINT('',(24.,-18.,-0.5));
#14299=CARTESIAN_POINT('',(24.,-18.,-0.5));
#14300=CARTESIAN_POINT('',(24.,-18.,0.));
#14301=CARTESIAN_POINT('',(24.,-18.,0.));
#14302=CARTESIAN_POINT('',(24.,-18.,-0.5));
#14303=CARTESIAN_POINT('Origin',(22.,-18.,-0.5));
#14304=CARTESIAN_POINT('',(22.,-18.,-0.5));
#14305=CARTESIAN_POINT('',(22.,-18.,-0.5));
#14306=CARTESIAN_POINT('',(22.,-18.,0.));
#14307=CARTESIAN_POINT('',(22.,-18.,0.));
#14308=CARTESIAN_POINT('',(22.,-18.,-0.5));
#14309=CARTESIAN_POINT('Origin',(22.,9.,-0.5));
#14310=CARTESIAN_POINT('',(22.,9.,-0.5));
#14311=CARTESIAN_POINT('',(22.,9.,0.));
#14312=CARTESIAN_POINT('Origin',(23.,-4.5,0.));
#14313=CARTESIAN_POINT('Origin',(23.,-4.5,-0.5));
#17213=UNCERTAINTY_MEASURE_WITH_UNIT(LENGTH_MEASURE(0.001),#17323,
'DISTANCE_ACCURACY_VALUE',
'Maximum model space distance between geometric entities at asserted c
onnectivities');
#17261=UNCERTAINTY_MEASURE_WITH_UNIT(LENGTH_MEASURE(0.001),#17323,
'DISTANCE_ACCURACY_VALUE',
'Maximum model space distance between geometric entities at asserted c
onnectivities');
#17274=(
GEOMETRIC_REPRESENTATION_CONTEXT(3)
GLOBAL_UNCERTAINTY_ASSIGNED_CONTEXT((#17213))
GLOBAL_UNIT_ASSIGNED_CONTEXT((#17323,#17325,#17326))
REPRESENTATION_CONTEXT('','3D')
);
#17322=(
GEOMETRIC_REPRESENTATION_CONTEXT(3)
GLOBAL_UNCERTAINTY_ASSIGNED_CONTEXT((#17261))
GLOBAL_UNIT_ASSIGNED_CONTEXT((#17323,#17325,#17326))
REPRESENTATION_CONTEXT('','3D')
);
#17323=(
LENGTH_UNIT()
NAMED_UNIT(*)
SI_UNIT(.CENTI.,.METRE.)
);
#17325=(
NAMED_UNIT(*)
PLANE_ANGLE_UNIT()
SI_UNIT($,.RADIAN.)
);
#17326=(
NAMED_UNIT(*)
SI_UNIT($,.STERADIAN.)
SOLID_ANGLE_UNIT()
);
#17339=SHAPE_DEFINITION_REPRESENTATION(#17399,#17570);
#17399=PRODUCT_DEFINITION_SHAPE('',$,#17631);
#17570=SHAPE_REPRESENTATION('',(#9939),#17274);
#17618=PRODUCT_DEFINITION_CONTEXT('part definition',#17800,'design');
#17631=PRODUCT_DEFINITION('Foot strip (1)','Foot strip (1)',#17691,#17618);
#17691=PRODUCT_DEFINITION_FORMATION('',$,#17814);
#17800=APPLICATION_CONTEXT(
'Core Data for Automotive Mechanical Design Process');
#17801=PRODUCT_CONTEXT('part definition',#17800,'mechanical');
#17814=PRODUCT('Foot strip (1)','Foot strip (1)','Foot strip (1)',(#17801));
#17911=COLOUR_RGB('Light Blue',0.38,0.62,0.78);
#17912=FILL_AREA_STYLE_COLOUR('',#17911);
#17913=FILL_AREA_STYLE('',(#17912));
#17914=SURFACE_STYLE_FILL_AREA(#17913);
#17915=SURFACE_SIDE_STYLE('',(#17914));
#17916=SURFACE_STYLE_USAGE(.BOTH.,#17915);
#17917=PRESENTATION_STYLE_ASSIGNMENT((#17916));
ENDSEC;
END-ISO-10303-21;
